ISO-10303-21;
HEADER;
/* Generated by software containing ST-Developer
 * from STEP Tools, Inc. (www.steptools.com) 
 */

FILE_DESCRIPTION(
/* description */ ('STEP AP214'),
/* implementation_level */ '2;1');

FILE_NAME(
/* name */ 'Ball Screw Nut.step',
/* time_stamp */ '2026-11-15T14:55:55-08:00',
/* author */ (''),
/* organization */ (''),
/* preprocessor_version */ 'ST-DEVELOPER v20.2',
/* originating_system */ 'Autodesk Translation Framework v15.17.0.0',
/* authorisation */ '');

FILE_SCHEMA (('AUTOMOTIVE_DESIGN { 1 0 10303 214 3 1 1 }'));
ENDSEC;

DATA;
#10=MECHANICAL_DESIGN_GEOMETRIC_PRESENTATION_REPRESENTATION('',(#928),#57079);
#639=TOROIDAL_SURFACE('',#25028,13.5,0.5);
#640=TOROIDAL_SURFACE('',#25034,23.,1.);
#641=TOROIDAL_SURFACE('',#25036,23.,1.);
#642=TOROIDAL_SURFACE('',#25042,23.,1.);
#643=TOROIDAL_SURFACE('',#25044,23.,1.);
#652=B_SPLINE_CURVE_WITH_KNOTS('',3,(#34902,#34903,#34904,#34905,#34906,
#34907,#34908,#34909,#34910,#34911,#34912,#34913,#34914,#34915,#34916,#34917,
#34918,#34919,#34920,#34921,#34922,#34923,#34924,#34925,#34926,#34927,#34928,
#34929,#34930,#34931,#34932,#34933,#34934,#34935),.UNSPECIFIED.,.T.,.F.,
(4,2,2,2,2,2,2,2,2,2,2,2,2,2,2,2,4),(-1.49374524883065,-1.40036599345989,
-1.30698673808914,-1.21364783735606,-1.12030893662298,-1.02697003588991,
-0.933631135156828,-0.840251879786076,-0.746872624415323,-0.65349336904457,
-0.560114113673817,-0.466775212940739,-0.373436312207661,-0.280097411474584,
-0.186758510741506,-0.0933792553707528,0.),.UNSPECIFIED.);
#653=B_SPLINE_CURVE_WITH_KNOTS('',3,(#34938,#34939,#34940,#34941,#34942,
#34943,#34944,#34945,#34946,#34947,#34948,#34949,#34950,#34951,#34952,#34953,
#34954,#34955,#34956,#34957,#34958,#34959,#34960,#34961,#34962,#34963,#34964,
#34965,#34966,#34967,#34968,#34969,#34970,#34971),.UNSPECIFIED.,.T.,.F.,
(4,2,2,2,2,2,2,2,2,2,2,2,2,2,2,2,4),(-1.48285153280719,-1.39017313824889,
-1.2974947436906,-1.204816696648,-1.11213864960539,-1.01946060256279,-0.926782555520185,
-0.83410416096189,-0.741425766403595,-0.6487473718453,-0.556068977287005,
-0.463390930244401,-0.370712883201798,-0.278034836159194,-0.18535678911659,
-0.0926783945582951,0.),.UNSPECIFIED.);
#654=B_SPLINE_CURVE_WITH_KNOTS('',3,(#35059,#35060,#35061,#35062,#35063,
#35064,#35065,#35066,#35067,#35068),.UNSPECIFIED.,.F.,.F.,(4,2,2,2,4),(-0.928911626390741,
-0.898926291162783,-0.857409357377827,-0.796302001537034,-0.707624607638868),
 .UNSPECIFIED.);
#655=B_SPLINE_CURVE_WITH_KNOTS('',3,(#35071,#35072,#35073,#35074,#35075,
#35076,#35077,#35078,#35079,#35080),.UNSPECIFIED.,.F.,.F.,(4,2,2,2,4),(-0.221287018750753,
-0.132609624853036,-0.0715022690125521,-0.0299853352278067,0.),
 .UNSPECIFIED.);
#656=B_SPLINE_CURVE_WITH_KNOTS('',3,(#35083,#35084,#35085,#35086,#35087,
#35088,#35089,#35090,#35091,#35092),.UNSPECIFIED.,.F.,.F.,(4,2,2,2,4),(-0.221287018750753,
-0.132609624853036,-0.0715022690125519,-0.0299853352278066,0.),
 .UNSPECIFIED.);
#657=B_SPLINE_CURVE_WITH_KNOTS('',3,(#35094,#35095,#35096,#35097,#35098,
#35099,#35100,#35101,#35102,#35103),.UNSPECIFIED.,.F.,.F.,(4,2,2,2,4),(-0.928911626390741,
-0.898926291162935,-0.857409357378189,-0.796302001537705,-0.707624607639988),
 .UNSPECIFIED.);
#658=B_SPLINE_CURVE_WITH_KNOTS('',3,(#35119,#35120,#35121,#35122,#35123,
#35124,#35125,#35126,#35127,#35128),.UNSPECIFIED.,.F.,.F.,(4,2,2,2,4),(-0.221287018750753,
-0.132609624853036,-0.071502269012552,-0.0299853352278066,2.77555756156289E-17),
 .UNSPECIFIED.);
#659=B_SPLINE_CURVE_WITH_KNOTS('',3,(#35131,#35132,#35133,#35134,#35135,
#35136,#35137,#35138,#35139,#35140),.UNSPECIFIED.,.F.,.F.,(4,2,2,2,4),(-0.928911626390742,
-0.898926291162935,-0.857409357378189,-0.796302001537705,-0.707624607639988),
 .UNSPECIFIED.);
#660=B_SPLINE_CURVE_WITH_KNOTS('',3,(#35143,#35144,#35145,#35146,#35147,
#35148,#35149,#35150,#35151,#35152),.UNSPECIFIED.,.F.,.F.,(4,2,2,2,4),(-0.928911626390739,
-0.898926291162933,-0.857409357378188,-0.796302001537705,-0.707624607639989),
 .UNSPECIFIED.);
#661=B_SPLINE_CURVE_WITH_KNOTS('',3,(#35154,#35155,#35156,#35157,#35158,
#35159,#35160,#35161,#35162,#35163),.UNSPECIFIED.,.F.,.F.,(4,2,2,2,4),(-0.221287018750753,
-0.132609624853036,-0.0715022690125519,-0.0299853352278065,0.),
 .UNSPECIFIED.);
#870=SHAPE_REPRESENTATION_RELATIONSHIP('SRR','None',#57254,#899);
#899=ADVANCED_BREP_SHAPE_REPRESENTATION('',(#965),#57046);
#928=STYLED_ITEM('',(#57444),#965);
#965=MANIFOLD_SOLID_BREP('Body1',#24528);
#1025=FACE_BOUND('',#3621,.T.);
#1026=FACE_BOUND('',#3626,.T.);
#1027=FACE_BOUND('',#3627,.T.);
#1028=FACE_BOUND('',#3628,.T.);
#1029=FACE_BOUND('',#3629,.T.);
#1030=FACE_BOUND('',#3630,.T.);
#1031=FACE_BOUND('',#3631,.T.);
#1032=FACE_BOUND('',#3632,.T.);
#1033=FACE_BOUND('',#3636,.T.);
#1034=FACE_BOUND('',#3641,.T.);
#1035=FACE_BOUND('',#3642,.T.);
#1036=FACE_BOUND('',#3643,.T.);
#1037=FACE_BOUND('',#3644,.T.);
#1038=FACE_BOUND('',#3645,.T.);
#1039=FACE_BOUND('',#3646,.T.);
#1040=FACE_BOUND('',#3647,.T.);
#1041=FACE_BOUND('',#3649,.T.);
#1042=FACE_BOUND('',#3651,.T.);
#1043=FACE_BOUND('',#3653,.T.);
#1044=FACE_BOUND('',#3655,.T.);
#1045=FACE_BOUND('',#3657,.T.);
#1362=PLANE('',#25031);
#1363=PLANE('',#25046);
#1364=PLANE('',#25047);
#1365=PLANE('',#25048);
#1366=PLANE('',#25049);
#1367=PLANE('',#25050);
#1368=PLANE('',#25051);
#1369=PLANE('',#25052);
#1370=PLANE('',#25053);
#2210=FACE_OUTER_BOUND('',#3610,.T.);
#2211=FACE_OUTER_BOUND('',#3611,.T.);
#2212=FACE_OUTER_BOUND('',#3612,.T.);
#2213=FACE_OUTER_BOUND('',#3613,.T.);
#2214=FACE_OUTER_BOUND('',#3614,.T.);
#2215=FACE_OUTER_BOUND('',#3615,.T.);
#2216=FACE_OUTER_BOUND('',#3616,.T.);
#2217=FACE_OUTER_BOUND('',#3617,.T.);
#2218=FACE_OUTER_BOUND('',#3618,.T.);
#2219=FACE_OUTER_BOUND('',#3619,.T.);
#2220=FACE_OUTER_BOUND('',#3620,.T.);
#2221=FACE_OUTER_BOUND('',#3622,.T.);
#2222=FACE_OUTER_BOUND('',#3623,.T.);
#2223=FACE_OUTER_BOUND('',#3624,.T.);
#2224=FACE_OUTER_BOUND('',#3625,.T.);
#2225=FACE_OUTER_BOUND('',#3633,.T.);
#2226=FACE_OUTER_BOUND('',#3634,.T.);
#2227=FACE_OUTER_BOUND('',#3635,.T.);
#2228=FACE_OUTER_BOUND('',#3637,.T.);
#2229=FACE_OUTER_BOUND('',#3638,.T.);
#2230=FACE_OUTER_BOUND('',#3639,.T.);
#2231=FACE_OUTER_BOUND('',#3640,.T.);
#2232=FACE_OUTER_BOUND('',#3648,.T.);
#2233=FACE_OUTER_BOUND('',#3650,.T.);
#2234=FACE_OUTER_BOUND('',#3652,.T.);
#2235=FACE_OUTER_BOUND('',#3654,.T.);
#2236=FACE_OUTER_BOUND('',#3656,.T.);
#2237=FACE_OUTER_BOUND('',#3658,.T.);
#2238=FACE_OUTER_BOUND('',#3659,.T.);
#3610=EDGE_LOOP('',(#16142,#16143,#16144,#16145));
#3611=EDGE_LOOP('',(#16146,#16147,#16148,#16149));
#3612=EDGE_LOOP('',(#16150,#16151,#16152,#16153));
#3613=EDGE_LOOP('',(#16154,#16155,#16156,#16157));
#3614=EDGE_LOOP('',(#16158,#16159,#16160,#16161));
#3615=EDGE_LOOP('',(#16162,#16163,#16164,#16165));
#3616=EDGE_LOOP('',(#16166,#16167,#16168,#16169));
#3617=EDGE_LOOP('',(#16170,#16171,#16172,#16173));
#3618=EDGE_LOOP('',(#16174,#16175,#16176,#16177));
#3619=EDGE_LOOP('',(#16178,#16179,#16180,#16181));
#3620=EDGE_LOOP('',(#16182,#16183,#16184,#16185));
#3621=EDGE_LOOP('',(#16186));
#3622=EDGE_LOOP('',(#16187,#16188,#16189,#16190));
#3623=EDGE_LOOP('',(#16191,#16192,#16193,#16194));
#3624=EDGE_LOOP('',(#16195,#16196,#16197,#16198));
#3625=EDGE_LOOP('',(#16199,#16200,#16201,#16202));
#3626=EDGE_LOOP('',(#16203));
#3627=EDGE_LOOP('',(#16204));
#3628=EDGE_LOOP('',(#16205));
#3629=EDGE_LOOP('',(#16206));
#3630=EDGE_LOOP('',(#16207));
#3631=EDGE_LOOP('',(#16208));
#3632=EDGE_LOOP('',(#16209));
#3633=EDGE_LOOP('',(#16210,#16211,#16212,#16213));
#3634=EDGE_LOOP('',(#16214,#16215,#16216,#16217));
#3635=EDGE_LOOP('',(#16218,#16219,#16220,#16221));
#3636=EDGE_LOOP('',(#16222));
#3637=EDGE_LOOP('',(#16223,#16224,#16225,#16226));
#3638=EDGE_LOOP('',(#16227,#16228,#16229,#16230));
#3639=EDGE_LOOP('',(#16231,#16232,#16233,#16234));
#3640=EDGE_LOOP('',(#16235,#16236,#16237,#16238));
#3641=EDGE_LOOP('',(#16239));
#3642=EDGE_LOOP('',(#16240));
#3643=EDGE_LOOP('',(#16241));
#3644=EDGE_LOOP('',(#16242));
#3645=EDGE_LOOP('',(#16243));
#3646=EDGE_LOOP('',(#16244));
#3647=EDGE_LOOP('',(#16245));
#3648=EDGE_LOOP('',(#16246));
#3649=EDGE_LOOP('',(#16247));
#3650=EDGE_LOOP('',(#16248));
#3651=EDGE_LOOP('',(#16249));
#3652=EDGE_LOOP('',(#16250));
#3653=EDGE_LOOP('',(#16251));
#3654=EDGE_LOOP('',(#16252));
#3655=EDGE_LOOP('',(#16253));
#3656=EDGE_LOOP('',(#16254));
#3657=EDGE_LOOP('',(#16255));
#3658=EDGE_LOOP('',(#16256,#16257,#16258,#16259,#16260,#16261,#16262,#16263));
#3659=EDGE_LOOP('',(#16264,#16265,#16266,#16267,#16268,#16269,#16270,#16271));
#5310=LINE('',#34937,#7277);
#5311=LINE('',#34976,#7278);
#5312=LINE('',#34982,#7279);
#5313=LINE('',#34988,#7280);
#5314=LINE('',#34994,#7281);
#5315=LINE('',#35000,#7282);
#5316=LINE('',#35006,#7283);
#5317=LINE('',#35012,#7284);
#5318=LINE('',#35018,#7285);
#5319=LINE('',#35024,#7286);
#5320=LINE('',#35030,#7287);
#5321=LINE('',#35036,#7288);
#5322=LINE('',#35042,#7289);
#5323=LINE('',#35051,#7290);
#5324=LINE('',#35055,#7291);
#5325=LINE('',#35107,#7292);
#5326=LINE('',#35110,#7293);
#5327=LINE('',#35113,#7294);
#5328=LINE('',#35115,#7295);
#5329=LINE('',#35166,#7296);
#5330=LINE('',#35167,#7297);
#7277=VECTOR('',#27754,2.45849999999999);
#7278=VECTOR('',#27759,2.74999999999999);
#7279=VECTOR('',#27766,2.74999999999999);
#7280=VECTOR('',#27773,2.74999999999999);
#7281=VECTOR('',#27780,2.74999999999999);
#7282=VECTOR('',#27787,2.74999999999999);
#7283=VECTOR('',#27794,2.74999999999999);
#7284=VECTOR('',#27801,14.);
#7285=VECTOR('',#27808,11.);
#7286=VECTOR('',#27815,10.75);
#7287=VECTOR('',#27822,7.5);
#7288=VECTOR('',#27829,10.75);
#7289=VECTOR('',#27836,11.);
#7290=VECTOR('',#27847,1000.);
#7291=VECTOR('',#27850,1000.);
#7292=VECTOR('',#27863,1000.);
#7293=VECTOR('',#27866,1000.);
#7294=VECTOR('',#27869,1000.);
#7295=VECTOR('',#27870,1000.);
#7296=VECTOR('',#27883,1000.);
#7297=VECTOR('',#27884,1000.);
#9236=CIRCLE('',#24993,2.74999999999999);
#9237=CIRCLE('',#24994,2.75);
#9238=CIRCLE('',#24996,2.74999999999999);
#9239=CIRCLE('',#24997,2.75);
#9240=CIRCLE('',#24999,2.74999999999999);
#9241=CIRCLE('',#25000,2.75);
#9242=CIRCLE('',#25002,2.74999999999999);
#9243=CIRCLE('',#25003,2.75);
#9244=CIRCLE('',#25005,2.74999999999999);
#9245=CIRCLE('',#25006,2.75);
#9246=CIRCLE('',#25008,2.74999999999999);
#9247=CIRCLE('',#25009,2.75);
#9248=CIRCLE('',#25011,14.);
#9249=CIRCLE('',#25012,14.);
#9250=CIRCLE('',#25014,11.);
#9251=CIRCLE('',#25015,11.);
#9252=CIRCLE('',#25017,10.75);
#9253=CIRCLE('',#25018,10.75);
#9254=CIRCLE('',#25020,7.5);
#9255=CIRCLE('',#25021,7.5);
#9256=CIRCLE('',#25023,10.75);
#9257=CIRCLE('',#25024,10.75);
#9258=CIRCLE('',#25026,11.);
#9259=CIRCLE('',#25027,11.);
#9260=CIRCLE('',#25029,13.5);
#9261=CIRCLE('',#25030,0.5);
#9262=CIRCLE('',#25032,23.);
#9263=CIRCLE('',#25033,23.);
#9264=CIRCLE('',#25035,24.);
#9265=CIRCLE('',#25037,24.);
#9266=CIRCLE('',#25039,24.);
#9267=CIRCLE('',#25041,24.);
#9268=CIRCLE('',#25043,23.);
#9269=CIRCLE('',#25045,23.);
#10354=VERTEX_POINT('',#34901);
#10355=VERTEX_POINT('',#34936);
#10356=VERTEX_POINT('',#34973);
#10357=VERTEX_POINT('',#34975);
#10358=VERTEX_POINT('',#34979);
#10359=VERTEX_POINT('',#34981);
#10360=VERTEX_POINT('',#34985);
#10361=VERTEX_POINT('',#34987);
#10362=VERTEX_POINT('',#34991);
#10363=VERTEX_POINT('',#34993);
#10364=VERTEX_POINT('',#34997);
#10365=VERTEX_POINT('',#34999);
#10366=VERTEX_POINT('',#35003);
#10367=VERTEX_POINT('',#35005);
#10368=VERTEX_POINT('',#35009);
#10369=VERTEX_POINT('',#35011);
#10370=VERTEX_POINT('',#35015);
#10371=VERTEX_POINT('',#35017);
#10372=VERTEX_POINT('',#35021);
#10373=VERTEX_POINT('',#35023);
#10374=VERTEX_POINT('',#35027);
#10375=VERTEX_POINT('',#35029);
#10376=VERTEX_POINT('',#35033);
#10377=VERTEX_POINT('',#35035);
#10378=VERTEX_POINT('',#35039);
#10379=VERTEX_POINT('',#35041);
#10380=VERTEX_POINT('',#35045);
#10381=VERTEX_POINT('',#35049);
#10382=VERTEX_POINT('',#35050);
#10383=VERTEX_POINT('',#35052);
#10384=VERTEX_POINT('',#35054);
#10385=VERTEX_POINT('',#35058);
#10386=VERTEX_POINT('',#35069);
#10387=VERTEX_POINT('',#35082);
#10388=VERTEX_POINT('',#35093);
#10389=VERTEX_POINT('',#35106);
#10390=VERTEX_POINT('',#35108);
#10391=VERTEX_POINT('',#35112);
#10392=VERTEX_POINT('',#35114);
#10393=VERTEX_POINT('',#35118);
#10394=VERTEX_POINT('',#35129);
#10395=VERTEX_POINT('',#35142);
#10396=VERTEX_POINT('',#35153);
#12616=EDGE_CURVE('',#10354,#10354,#652,.T.);
#12617=EDGE_CURVE('',#10354,#10355,#5310,.T.);
#12618=EDGE_CURVE('',#10355,#10355,#653,.T.);
#12619=EDGE_CURVE('',#10356,#10356,#9236,.T.);
#12620=EDGE_CURVE('',#10356,#10357,#5311,.T.);
#12621=EDGE_CURVE('',#10357,#10357,#9237,.T.);
#12622=EDGE_CURVE('',#10358,#10358,#9238,.T.);
#12623=EDGE_CURVE('',#10358,#10359,#5312,.T.);
#12624=EDGE_CURVE('',#10359,#10359,#9239,.T.);
#12625=EDGE_CURVE('',#10360,#10360,#9240,.T.);
#12626=EDGE_CURVE('',#10360,#10361,#5313,.T.);
#12627=EDGE_CURVE('',#10361,#10361,#9241,.T.);
#12628=EDGE_CURVE('',#10362,#10362,#9242,.T.);
#12629=EDGE_CURVE('',#10362,#10363,#5314,.T.);
#12630=EDGE_CURVE('',#10363,#10363,#9243,.T.);
#12631=EDGE_CURVE('',#10364,#10364,#9244,.T.);
#12632=EDGE_CURVE('',#10364,#10365,#5315,.T.);
#12633=EDGE_CURVE('',#10365,#10365,#9245,.T.);
#12634=EDGE_CURVE('',#10366,#10366,#9246,.T.);
#12635=EDGE_CURVE('',#10366,#10367,#5316,.T.);
#12636=EDGE_CURVE('',#10367,#10367,#9247,.T.);
#12637=EDGE_CURVE('',#10368,#10368,#9248,.T.);
#12638=EDGE_CURVE('',#10368,#10369,#5317,.T.);
#12639=EDGE_CURVE('',#10369,#10369,#9249,.T.);
#12640=EDGE_CURVE('',#10370,#10370,#9250,.T.);
#12641=EDGE_CURVE('',#10370,#10371,#5318,.T.);
#12642=EDGE_CURVE('',#10371,#10371,#9251,.T.);
#12643=EDGE_CURVE('',#10372,#10372,#9252,.T.);
#12644=EDGE_CURVE('',#10372,#10373,#5319,.T.);
#12645=EDGE_CURVE('',#10373,#10373,#9253,.T.);
#12646=EDGE_CURVE('',#10374,#10374,#9254,.T.);
#12647=EDGE_CURVE('',#10374,#10375,#5320,.T.);
#12648=EDGE_CURVE('',#10375,#10375,#9255,.T.);
#12649=EDGE_CURVE('',#10376,#10376,#9256,.T.);
#12650=EDGE_CURVE('',#10376,#10377,#5321,.T.);
#12651=EDGE_CURVE('',#10377,#10377,#9257,.T.);
#12652=EDGE_CURVE('',#10378,#10378,#9258,.T.);
#12653=EDGE_CURVE('',#10378,#10379,#5322,.T.);
#12654=EDGE_CURVE('',#10379,#10379,#9259,.T.);
#12655=EDGE_CURVE('',#10380,#10380,#9260,.T.);
#12656=EDGE_CURVE('',#10380,#10368,#9261,.T.);
#12657=EDGE_CURVE('',#10381,#10382,#5323,.T.);
#12658=EDGE_CURVE('',#10383,#10382,#9262,.T.);
#12659=EDGE_CURVE('',#10383,#10384,#5324,.T.);
#12660=EDGE_CURVE('',#10381,#10384,#9263,.T.);
#12661=EDGE_CURVE('',#10385,#10382,#654,.T.);
#12662=EDGE_CURVE('',#10386,#10385,#9264,.T.);
#12663=EDGE_CURVE('',#10383,#10386,#655,.T.);
#12664=EDGE_CURVE('',#10381,#10387,#656,.T.);
#12665=EDGE_CURVE('',#10388,#10384,#657,.T.);
#12666=EDGE_CURVE('',#10387,#10388,#9265,.T.);
#12667=EDGE_CURVE('',#10389,#10388,#5325,.T.);
#12668=EDGE_CURVE('',#10390,#10389,#9266,.T.);
#12669=EDGE_CURVE('',#10387,#10390,#5326,.T.);
#12670=EDGE_CURVE('',#10386,#10391,#5327,.T.);
#12671=EDGE_CURVE('',#10392,#10385,#5328,.T.);
#12672=EDGE_CURVE('',#10391,#10392,#9267,.T.);
#12673=EDGE_CURVE('',#10393,#10392,#658,.T.);
#12674=EDGE_CURVE('',#10394,#10393,#9268,.T.);
#12675=EDGE_CURVE('',#10391,#10394,#659,.T.);
#12676=EDGE_CURVE('',#10390,#10395,#660,.T.);
#12677=EDGE_CURVE('',#10396,#10389,#661,.T.);
#12678=EDGE_CURVE('',#10395,#10396,#9269,.T.);
#12679=EDGE_CURVE('',#10395,#10393,#5329,.T.);
#12680=EDGE_CURVE('',#10394,#10396,#5330,.T.);
#16142=ORIENTED_EDGE('',*,*,#12616,.F.);
#16143=ORIENTED_EDGE('',*,*,#12617,.T.);
#16144=ORIENTED_EDGE('',*,*,#12618,.F.);
#16145=ORIENTED_EDGE('',*,*,#12617,.F.);
#16146=ORIENTED_EDGE('',*,*,#12619,.F.);
#16147=ORIENTED_EDGE('',*,*,#12620,.T.);
#16148=ORIENTED_EDGE('',*,*,#12621,.T.);
#16149=ORIENTED_EDGE('',*,*,#12620,.F.);
#16150=ORIENTED_EDGE('',*,*,#12622,.F.);
#16151=ORIENTED_EDGE('',*,*,#12623,.T.);
#16152=ORIENTED_EDGE('',*,*,#12624,.T.);
#16153=ORIENTED_EDGE('',*,*,#12623,.F.);
#16154=ORIENTED_EDGE('',*,*,#12625,.F.);
#16155=ORIENTED_EDGE('',*,*,#12626,.T.);
#16156=ORIENTED_EDGE('',*,*,#12627,.T.);
#16157=ORIENTED_EDGE('',*,*,#12626,.F.);
#16158=ORIENTED_EDGE('',*,*,#12628,.F.);
#16159=ORIENTED_EDGE('',*,*,#12629,.T.);
#16160=ORIENTED_EDGE('',*,*,#12630,.T.);
#16161=ORIENTED_EDGE('',*,*,#12629,.F.);
#16162=ORIENTED_EDGE('',*,*,#12631,.F.);
#16163=ORIENTED_EDGE('',*,*,#12632,.T.);
#16164=ORIENTED_EDGE('',*,*,#12633,.T.);
#16165=ORIENTED_EDGE('',*,*,#12632,.F.);
#16166=ORIENTED_EDGE('',*,*,#12634,.F.);
#16167=ORIENTED_EDGE('',*,*,#12635,.T.);
#16168=ORIENTED_EDGE('',*,*,#12636,.T.);
#16169=ORIENTED_EDGE('',*,*,#12635,.F.);
#16170=ORIENTED_EDGE('',*,*,#12637,.F.);
#16171=ORIENTED_EDGE('',*,*,#12638,.T.);
#16172=ORIENTED_EDGE('',*,*,#12639,.T.);
#16173=ORIENTED_EDGE('',*,*,#12638,.F.);
#16174=ORIENTED_EDGE('',*,*,#12640,.F.);
#16175=ORIENTED_EDGE('',*,*,#12641,.T.);
#16176=ORIENTED_EDGE('',*,*,#12642,.T.);
#16177=ORIENTED_EDGE('',*,*,#12641,.F.);
#16178=ORIENTED_EDGE('',*,*,#12643,.F.);
#16179=ORIENTED_EDGE('',*,*,#12644,.T.);
#16180=ORIENTED_EDGE('',*,*,#12645,.T.);
#16181=ORIENTED_EDGE('',*,*,#12644,.F.);
#16182=ORIENTED_EDGE('',*,*,#12646,.F.);
#16183=ORIENTED_EDGE('',*,*,#12647,.T.);
#16184=ORIENTED_EDGE('',*,*,#12648,.T.);
#16185=ORIENTED_EDGE('',*,*,#12647,.F.);
#16186=ORIENTED_EDGE('',*,*,#12616,.T.);
#16187=ORIENTED_EDGE('',*,*,#12649,.F.);
#16188=ORIENTED_EDGE('',*,*,#12650,.T.);
#16189=ORIENTED_EDGE('',*,*,#12651,.T.);
#16190=ORIENTED_EDGE('',*,*,#12650,.F.);
#16191=ORIENTED_EDGE('',*,*,#12652,.F.);
#16192=ORIENTED_EDGE('',*,*,#12653,.T.);
#16193=ORIENTED_EDGE('',*,*,#12654,.T.);
#16194=ORIENTED_EDGE('',*,*,#12653,.F.);
#16195=ORIENTED_EDGE('',*,*,#12655,.F.);
#16196=ORIENTED_EDGE('',*,*,#12656,.T.);
#16197=ORIENTED_EDGE('',*,*,#12637,.T.);
#16198=ORIENTED_EDGE('',*,*,#12656,.F.);
#16199=ORIENTED_EDGE('',*,*,#12657,.T.);
#16200=ORIENTED_EDGE('',*,*,#12658,.F.);
#16201=ORIENTED_EDGE('',*,*,#12659,.T.);
#16202=ORIENTED_EDGE('',*,*,#12660,.F.);
#16203=ORIENTED_EDGE('',*,*,#12621,.F.);
#16204=ORIENTED_EDGE('',*,*,#12624,.F.);
#16205=ORIENTED_EDGE('',*,*,#12627,.F.);
#16206=ORIENTED_EDGE('',*,*,#12630,.F.);
#16207=ORIENTED_EDGE('',*,*,#12633,.F.);
#16208=ORIENTED_EDGE('',*,*,#12636,.F.);
#16209=ORIENTED_EDGE('',*,*,#12640,.T.);
#16210=ORIENTED_EDGE('',*,*,#12661,.F.);
#16211=ORIENTED_EDGE('',*,*,#12662,.F.);
#16212=ORIENTED_EDGE('',*,*,#12663,.F.);
#16213=ORIENTED_EDGE('',*,*,#12658,.T.);
#16214=ORIENTED_EDGE('',*,*,#12664,.F.);
#16215=ORIENTED_EDGE('',*,*,#12660,.T.);
#16216=ORIENTED_EDGE('',*,*,#12665,.F.);
#16217=ORIENTED_EDGE('',*,*,#12666,.F.);
#16218=ORIENTED_EDGE('',*,*,#12667,.F.);
#16219=ORIENTED_EDGE('',*,*,#12668,.F.);
#16220=ORIENTED_EDGE('',*,*,#12669,.F.);
#16221=ORIENTED_EDGE('',*,*,#12666,.T.);
#16222=ORIENTED_EDGE('',*,*,#12618,.T.);
#16223=ORIENTED_EDGE('',*,*,#12670,.F.);
#16224=ORIENTED_EDGE('',*,*,#12662,.T.);
#16225=ORIENTED_EDGE('',*,*,#12671,.F.);
#16226=ORIENTED_EDGE('',*,*,#12672,.F.);
#16227=ORIENTED_EDGE('',*,*,#12673,.F.);
#16228=ORIENTED_EDGE('',*,*,#12674,.F.);
#16229=ORIENTED_EDGE('',*,*,#12675,.F.);
#16230=ORIENTED_EDGE('',*,*,#12672,.T.);
#16231=ORIENTED_EDGE('',*,*,#12676,.F.);
#16232=ORIENTED_EDGE('',*,*,#12668,.T.);
#16233=ORIENTED_EDGE('',*,*,#12677,.F.);
#16234=ORIENTED_EDGE('',*,*,#12678,.F.);
#16235=ORIENTED_EDGE('',*,*,#12679,.F.);
#16236=ORIENTED_EDGE('',*,*,#12678,.T.);
#16237=ORIENTED_EDGE('',*,*,#12680,.F.);
#16238=ORIENTED_EDGE('',*,*,#12674,.T.);
#16239=ORIENTED_EDGE('',*,*,#12619,.T.);
#16240=ORIENTED_EDGE('',*,*,#12622,.T.);
#16241=ORIENTED_EDGE('',*,*,#12625,.T.);
#16242=ORIENTED_EDGE('',*,*,#12628,.T.);
#16243=ORIENTED_EDGE('',*,*,#12631,.T.);
#16244=ORIENTED_EDGE('',*,*,#12634,.T.);
#16245=ORIENTED_EDGE('',*,*,#12639,.F.);
#16246=ORIENTED_EDGE('',*,*,#12655,.T.);
#16247=ORIENTED_EDGE('',*,*,#12654,.F.);
#16248=ORIENTED_EDGE('',*,*,#12652,.T.);
#16249=ORIENTED_EDGE('',*,*,#12651,.F.);
#16250=ORIENTED_EDGE('',*,*,#12649,.T.);
#16251=ORIENTED_EDGE('',*,*,#12648,.F.);
#16252=ORIENTED_EDGE('',*,*,#12645,.F.);
#16253=ORIENTED_EDGE('',*,*,#12646,.T.);
#16254=ORIENTED_EDGE('',*,*,#12642,.F.);
#16255=ORIENTED_EDGE('',*,*,#12643,.T.);
#16256=ORIENTED_EDGE('',*,*,#12663,.T.);
#16257=ORIENTED_EDGE('',*,*,#12670,.T.);
#16258=ORIENTED_EDGE('',*,*,#12675,.T.);
#16259=ORIENTED_EDGE('',*,*,#12680,.T.);
#16260=ORIENTED_EDGE('',*,*,#12677,.T.);
#16261=ORIENTED_EDGE('',*,*,#12667,.T.);
#16262=ORIENTED_EDGE('',*,*,#12665,.T.);
#16263=ORIENTED_EDGE('',*,*,#12659,.F.);
#16264=ORIENTED_EDGE('',*,*,#12661,.T.);
#16265=ORIENTED_EDGE('',*,*,#12657,.F.);
#16266=ORIENTED_EDGE('',*,*,#12664,.T.);
#16267=ORIENTED_EDGE('',*,*,#12669,.T.);
#16268=ORIENTED_EDGE('',*,*,#12676,.T.);
#16269=ORIENTED_EDGE('',*,*,#12679,.T.);
#16270=ORIENTED_EDGE('',*,*,#12673,.T.);
#16271=ORIENTED_EDGE('',*,*,#12671,.T.);
#22761=CYLINDRICAL_SURFACE('',#24991,2.45849999999999);
#22762=CYLINDRICAL_SURFACE('',#24992,2.74999999999999);
#22763=CYLINDRICAL_SURFACE('',#24995,2.74999999999999);
#22764=CYLINDRICAL_SURFACE('',#24998,2.74999999999999);
#22765=CYLINDRICAL_SURFACE('',#25001,2.74999999999999);
#22766=CYLINDRICAL_SURFACE('',#25004,2.74999999999999);
#22767=CYLINDRICAL_SURFACE('',#25007,2.74999999999999);
#22768=CYLINDRICAL_SURFACE('',#25010,14.);
#22769=CYLINDRICAL_SURFACE('',#25013,11.);
#22770=CYLINDRICAL_SURFACE('',#25016,10.75);
#22771=CYLINDRICAL_SURFACE('',#25019,7.5);
#22772=CYLINDRICAL_SURFACE('',#25022,10.75);
#22773=CYLINDRICAL_SURFACE('',#25025,11.);
#22774=CYLINDRICAL_SURFACE('',#25038,24.);
#22775=CYLINDRICAL_SURFACE('',#25040,24.);
#23202=ADVANCED_FACE('',(#2210),#22761,.F.);
#23203=ADVANCED_FACE('',(#2211),#22762,.F.);
#23204=ADVANCED_FACE('',(#2212),#22763,.F.);
#23205=ADVANCED_FACE('',(#2213),#22764,.F.);
#23206=ADVANCED_FACE('',(#2214),#22765,.F.);
#23207=ADVANCED_FACE('',(#2215),#22766,.F.);
#23208=ADVANCED_FACE('',(#2216),#22767,.F.);
#23209=ADVANCED_FACE('',(#2217),#22768,.T.);
#23210=ADVANCED_FACE('',(#2218),#22769,.F.);
#23211=ADVANCED_FACE('',(#2219),#22770,.T.);
#23212=ADVANCED_FACE('',(#2220,#1025),#22771,.F.);
#23213=ADVANCED_FACE('',(#2221),#22772,.T.);
#23214=ADVANCED_FACE('',(#2222),#22773,.F.);
#23215=ADVANCED_FACE('',(#2223),#639,.T.);
#23216=ADVANCED_FACE('',(#2224,#1026,#1027,#1028,#1029,#1030,#1031,#1032),
#1362,.F.);
#23217=ADVANCED_FACE('',(#2225),#640,.T.);
#23218=ADVANCED_FACE('',(#2226),#641,.T.);
#23219=ADVANCED_FACE('',(#2227,#1033),#22774,.T.);
#23220=ADVANCED_FACE('',(#2228),#22775,.T.);
#23221=ADVANCED_FACE('',(#2229),#642,.T.);
#23222=ADVANCED_FACE('',(#2230),#643,.T.);
#23223=ADVANCED_FACE('',(#2231,#1034,#1035,#1036,#1037,#1038,#1039,#1040),
#1363,.F.);
#23224=ADVANCED_FACE('',(#2232,#1041),#1364,.F.);
#23225=ADVANCED_FACE('',(#2233,#1042),#1365,.F.);
#23226=ADVANCED_FACE('',(#2234,#1043),#1366,.F.);
#23227=ADVANCED_FACE('',(#2235,#1044),#1367,.F.);
#23228=ADVANCED_FACE('',(#2236,#1045),#1368,.F.);
#23229=ADVANCED_FACE('',(#2237),#1369,.T.);
#23230=ADVANCED_FACE('',(#2238),#1370,.T.);
#24528=CLOSED_SHELL('',(#23202,#23203,#23204,#23205,#23206,#23207,#23208,
#23209,#23210,#23211,#23212,#23213,#23214,#23215,#23216,#23217,#23218,#23219,
#23220,#23221,#23222,#23223,#23224,#23225,#23226,#23227,#23228,#23229,#23230));
#24990=AXIS2_PLACEMENT_3D('',#34899,#27750,#27751);
#24991=AXIS2_PLACEMENT_3D('',#34900,#27752,#27753);
#24992=AXIS2_PLACEMENT_3D('',#34972,#27755,#27756);
#24993=AXIS2_PLACEMENT_3D('',#34974,#27757,#27758);
#24994=AXIS2_PLACEMENT_3D('',#34977,#27760,#27761);
#24995=AXIS2_PLACEMENT_3D('',#34978,#27762,#27763);
#24996=AXIS2_PLACEMENT_3D('',#34980,#27764,#27765);
#24997=AXIS2_PLACEMENT_3D('',#34983,#27767,#27768);
#24998=AXIS2_PLACEMENT_3D('',#34984,#27769,#27770);
#24999=AXIS2_PLACEMENT_3D('',#34986,#27771,#27772);
#25000=AXIS2_PLACEMENT_3D('',#34989,#27774,#27775);
#25001=AXIS2_PLACEMENT_3D('',#34990,#27776,#27777);
#25002=AXIS2_PLACEMENT_3D('',#34992,#27778,#27779);
#25003=AXIS2_PLACEMENT_3D('',#34995,#27781,#27782);
#25004=AXIS2_PLACEMENT_3D('',#34996,#27783,#27784);
#25005=AXIS2_PLACEMENT_3D('',#34998,#27785,#27786);
#25006=AXIS2_PLACEMENT_3D('',#35001,#27788,#27789);
#25007=AXIS2_PLACEMENT_3D('',#35002,#27790,#27791);
#25008=AXIS2_PLACEMENT_3D('',#35004,#27792,#27793);
#25009=AXIS2_PLACEMENT_3D('',#35007,#27795,#27796);
#25010=AXIS2_PLACEMENT_3D('',#35008,#27797,#27798);
#25011=AXIS2_PLACEMENT_3D('',#35010,#27799,#27800);
#25012=AXIS2_PLACEMENT_3D('',#35013,#27802,#27803);
#25013=AXIS2_PLACEMENT_3D('',#35014,#27804,#27805);
#25014=AXIS2_PLACEMENT_3D('',#35016,#27806,#27807);
#25015=AXIS2_PLACEMENT_3D('',#35019,#27809,#27810);
#25016=AXIS2_PLACEMENT_3D('',#35020,#27811,#27812);
#25017=AXIS2_PLACEMENT_3D('',#35022,#27813,#27814);
#25018=AXIS2_PLACEMENT_3D('',#35025,#27816,#27817);
#25019=AXIS2_PLACEMENT_3D('',#35026,#27818,#27819);
#25020=AXIS2_PLACEMENT_3D('',#35028,#27820,#27821);
#25021=AXIS2_PLACEMENT_3D('',#35031,#27823,#27824);
#25022=AXIS2_PLACEMENT_3D('',#35032,#27825,#27826);
#25023=AXIS2_PLACEMENT_3D('',#35034,#27827,#27828);
#25024=AXIS2_PLACEMENT_3D('',#35037,#27830,#27831);
#25025=AXIS2_PLACEMENT_3D('',#35038,#27832,#27833);
#25026=AXIS2_PLACEMENT_3D('',#35040,#27834,#27835);
#25027=AXIS2_PLACEMENT_3D('',#35043,#27837,#27838);
#25028=AXIS2_PLACEMENT_3D('',#35044,#27839,#27840);
#25029=AXIS2_PLACEMENT_3D('',#35046,#27841,#27842);
#25030=AXIS2_PLACEMENT_3D('',#35047,#27843,#27844);
#25031=AXIS2_PLACEMENT_3D('',#35048,#27845,#27846);
#25032=AXIS2_PLACEMENT_3D('',#35053,#27848,#27849);
#25033=AXIS2_PLACEMENT_3D('',#35056,#27851,#27852);
#25034=AXIS2_PLACEMENT_3D('',#35057,#27853,#27854);
#25035=AXIS2_PLACEMENT_3D('',#35070,#27855,#27856);
#25036=AXIS2_PLACEMENT_3D('',#35081,#27857,#27858);
#25037=AXIS2_PLACEMENT_3D('',#35104,#27859,#27860);
#25038=AXIS2_PLACEMENT_3D('',#35105,#27861,#27862);
#25039=AXIS2_PLACEMENT_3D('',#35109,#27864,#27865);
#25040=AXIS2_PLACEMENT_3D('',#35111,#27867,#27868);
#25041=AXIS2_PLACEMENT_3D('',#35116,#27871,#27872);
#25042=AXIS2_PLACEMENT_3D('',#35117,#27873,#27874);
#25043=AXIS2_PLACEMENT_3D('',#35130,#27875,#27876);
#25044=AXIS2_PLACEMENT_3D('',#35141,#27877,#27878);
#25045=AXIS2_PLACEMENT_3D('',#35164,#27879,#27880);
#25046=AXIS2_PLACEMENT_3D('',#35165,#27881,#27882);
#25047=AXIS2_PLACEMENT_3D('',#35168,#27885,#27886);
#25048=AXIS2_PLACEMENT_3D('',#35169,#27887,#27888);
#25049=AXIS2_PLACEMENT_3D('',#35170,#27889,#27890);
#25050=AXIS2_PLACEMENT_3D('',#35171,#27891,#27892);
#25051=AXIS2_PLACEMENT_3D('',#35172,#27893,#27894);
#25052=AXIS2_PLACEMENT_3D('',#35173,#27895,#27896);
#25053=AXIS2_PLACEMENT_3D('',#35174,#27897,#27898);
#27750=DIRECTION('axis',(0.,0.,1.));
#27751=DIRECTION('refdir',(1.,0.,0.));
#27752=DIRECTION('center_axis',(0.,0.923879532511287,0.382683432365091));
#27753=DIRECTION('ref_axis',(0.,-0.382683432365091,0.923879532511286));
#27754=DIRECTION('',(0.,0.923879532511286,0.382683432365091));
#27755=DIRECTION('center_axis',(1.,0.,0.));
#27756=DIRECTION('ref_axis',(0.,0.,-1.));
#27757=DIRECTION('center_axis',(1.,0.,0.));
#27758=DIRECTION('ref_axis',(0.,0.,-1.));
#27759=DIRECTION('',(1.,0.,0.));
#27760=DIRECTION('center_axis',(1.,0.,0.));
#27761=DIRECTION('ref_axis',(0.,0.,-1.));
#27762=DIRECTION('center_axis',(1.,0.,0.));
#27763=DIRECTION('ref_axis',(0.,0.,-1.));
#27764=DIRECTION('center_axis',(1.,0.,0.));
#27765=DIRECTION('ref_axis',(0.,0.,-1.));
#27766=DIRECTION('',(1.,0.,0.));
#27767=DIRECTION('center_axis',(1.,0.,0.));
#27768=DIRECTION('ref_axis',(0.,0.,-1.));
#27769=DIRECTION('center_axis',(1.,0.,0.));
#27770=DIRECTION('ref_axis',(0.,0.,-1.));
#27771=DIRECTION('center_axis',(1.,0.,0.));
#27772=DIRECTION('ref_axis',(0.,0.,-1.));
#27773=DIRECTION('',(1.,0.,0.));
#27774=DIRECTION('center_axis',(1.,0.,0.));
#27775=DIRECTION('ref_axis',(0.,0.,-1.));
#27776=DIRECTION('center_axis',(1.,0.,0.));
#27777=DIRECTION('ref_axis',(0.,0.,-1.));
#27778=DIRECTION('center_axis',(1.,0.,0.));
#27779=DIRECTION('ref_axis',(0.,0.,-1.));
#27780=DIRECTION('',(1.,0.,0.));
#27781=DIRECTION('center_axis',(1.,0.,0.));
#27782=DIRECTION('ref_axis',(0.,0.,-1.));
#27783=DIRECTION('center_axis',(1.,0.,0.));
#27784=DIRECTION('ref_axis',(0.,0.,-1.));
#27785=DIRECTION('center_axis',(1.,0.,0.));
#27786=DIRECTION('ref_axis',(0.,0.,-1.));
#27787=DIRECTION('',(1.,0.,0.));
#27788=DIRECTION('center_axis',(1.,0.,0.));
#27789=DIRECTION('ref_axis',(0.,0.,-1.));
#27790=DIRECTION('center_axis',(1.,0.,0.));
#27791=DIRECTION('ref_axis',(0.,0.,-1.));
#27792=DIRECTION('center_axis',(1.,0.,0.));
#27793=DIRECTION('ref_axis',(0.,0.,-1.));
#27794=DIRECTION('',(1.,0.,0.));
#27795=DIRECTION('center_axis',(1.,0.,0.));
#27796=DIRECTION('ref_axis',(0.,0.,-1.));
#27797=DIRECTION('center_axis',(-1.,0.,0.));
#27798=DIRECTION('ref_axis',(0.,0.,1.));
#27799=DIRECTION('center_axis',(-1.,0.,0.));
#27800=DIRECTION('ref_axis',(0.,0.,1.));
#27801=DIRECTION('',(1.,0.,0.));
#27802=DIRECTION('center_axis',(-1.,0.,0.));
#27803=DIRECTION('ref_axis',(0.,0.,1.));
#27804=DIRECTION('center_axis',(-1.,0.,0.));
#27805=DIRECTION('ref_axis',(0.,0.,1.));
#27806=DIRECTION('center_axis',(-1.,0.,0.));
#27807=DIRECTION('ref_axis',(0.,0.,1.));
#27808=DIRECTION('',(-1.,0.,0.));
#27809=DIRECTION('center_axis',(-1.,0.,0.));
#27810=DIRECTION('ref_axis',(0.,0.,1.));
#27811=DIRECTION('center_axis',(-1.,0.,0.));
#27812=DIRECTION('ref_axis',(0.,0.,1.));
#27813=DIRECTION('center_axis',(-1.,0.,0.));
#27814=DIRECTION('ref_axis',(0.,0.,1.));
#27815=DIRECTION('',(1.,0.,0.));
#27816=DIRECTION('center_axis',(-1.,0.,0.));
#27817=DIRECTION('ref_axis',(0.,0.,1.));
#27818=DIRECTION('center_axis',(-1.,0.,0.));
#27819=DIRECTION('ref_axis',(0.,0.,1.));
#27820=DIRECTION('center_axis',(-1.,0.,0.));
#27821=DIRECTION('ref_axis',(0.,0.,1.));
#27822=DIRECTION('',(-1.,0.,0.));
#27823=DIRECTION('center_axis',(-1.,0.,0.));
#27824=DIRECTION('ref_axis',(0.,0.,1.));
#27825=DIRECTION('center_axis',(-1.,0.,0.));
#27826=DIRECTION('ref_axis',(0.,0.,1.));
#27827=DIRECTION('center_axis',(-1.,0.,0.));
#27828=DIRECTION('ref_axis',(0.,0.,1.));
#27829=DIRECTION('',(1.,0.,0.));
#27830=DIRECTION('center_axis',(-1.,0.,0.));
#27831=DIRECTION('ref_axis',(0.,0.,1.));
#27832=DIRECTION('center_axis',(-1.,0.,0.));
#27833=DIRECTION('ref_axis',(0.,0.,1.));
#27834=DIRECTION('center_axis',(-1.,0.,0.));
#27835=DIRECTION('ref_axis',(0.,0.,1.));
#27836=DIRECTION('',(-1.,0.,0.));
#27837=DIRECTION('center_axis',(-1.,0.,0.));
#27838=DIRECTION('ref_axis',(0.,0.,1.));
#27839=DIRECTION('center_axis',(-1.,0.,0.));
#27840=DIRECTION('ref_axis',(0.,0.,1.));
#27841=DIRECTION('center_axis',(-1.,0.,0.));
#27842=DIRECTION('ref_axis',(0.,0.,1.));
#27843=DIRECTION('center_axis',(0.,-1.,1.22464679914735E-16));
#27844=DIRECTION('ref_axis',(0.,-1.22464679914735E-16,-1.));
#27845=DIRECTION('center_axis',(-1.,0.,0.));
#27846=DIRECTION('ref_axis',(0.,0.,1.));
#27847=DIRECTION('',(0.,-1.,1.44560289664734E-16));
#27848=DIRECTION('center_axis',(-1.,0.,0.));
#27849=DIRECTION('ref_axis',(0.,0.,1.));
#27850=DIRECTION('',(0.,1.,1.44560289664734E-16));
#27851=DIRECTION('center_axis',(-1.,0.,0.));
#27852=DIRECTION('ref_axis',(0.,0.,1.));
#27853=DIRECTION('center_axis',(-1.,0.,0.));
#27854=DIRECTION('ref_axis',(0.,0.,1.));
#27855=DIRECTION('center_axis',(-1.,0.,0.));
#27856=DIRECTION('ref_axis',(0.,0.,1.));
#27857=DIRECTION('center_axis',(-1.,0.,0.));
#27858=DIRECTION('ref_axis',(0.,0.,1.));
#27859=DIRECTION('center_axis',(-1.,0.,0.));
#27860=DIRECTION('ref_axis',(0.,0.,1.));
#27861=DIRECTION('center_axis',(-1.,0.,0.));
#27862=DIRECTION('ref_axis',(0.,0.,1.));
#27863=DIRECTION('',(1.,0.,0.));
#27864=DIRECTION('center_axis',(-1.,0.,0.));
#27865=DIRECTION('ref_axis',(0.,0.,1.));
#27866=DIRECTION('',(-1.,0.,0.));
#27867=DIRECTION('center_axis',(-1.,0.,0.));
#27868=DIRECTION('ref_axis',(0.,0.,1.));
#27869=DIRECTION('',(-1.,0.,0.));
#27870=DIRECTION('',(1.,0.,0.));
#27871=DIRECTION('center_axis',(-1.,0.,0.));
#27872=DIRECTION('ref_axis',(0.,0.,1.));
#27873=DIRECTION('center_axis',(-1.,0.,0.));
#27874=DIRECTION('ref_axis',(0.,0.,1.));
#27875=DIRECTION('center_axis',(-1.,0.,0.));
#27876=DIRECTION('ref_axis',(0.,0.,1.));
#27877=DIRECTION('center_axis',(-1.,0.,0.));
#27878=DIRECTION('ref_axis',(0.,0.,1.));
#27879=DIRECTION('center_axis',(-1.,0.,0.));
#27880=DIRECTION('ref_axis',(0.,0.,1.));
#27881=DIRECTION('center_axis',(1.,0.,0.));
#27882=DIRECTION('ref_axis',(0.,0.,-1.));
#27883=DIRECTION('',(0.,-1.,1.44560289664734E-16));
#27884=DIRECTION('',(0.,1.,1.44560289664734E-16));
#27885=DIRECTION('center_axis',(1.,0.,0.));
#27886=DIRECTION('ref_axis',(0.,0.,-1.));
#27887=DIRECTION('center_axis',(1.,0.,0.));
#27888=DIRECTION('ref_axis',(0.,0.,-1.));
#27889=DIRECTION('center_axis',(1.,0.,0.));
#27890=DIRECTION('ref_axis',(0.,0.,-1.));
#27891=DIRECTION('center_axis',(-1.,0.,0.));
#27892=DIRECTION('ref_axis',(0.,0.,1.));
#27893=DIRECTION('center_axis',(-1.,0.,0.));
#27894=DIRECTION('ref_axis',(0.,0.,1.));
#27895=DIRECTION('center_axis',(0.,1.44560289664734E-16,-1.));
#27896=DIRECTION('ref_axis',(0.,1.,1.44560289664734E-16));
#27897=DIRECTION('center_axis',(0.,1.44560289664734E-16,1.));
#27898=DIRECTION('ref_axis',(0.,-1.,1.44560289664734E-16));
#34899=CARTESIAN_POINT('',(0.,0.,0.));
#34900=CARTESIAN_POINT('Origin',(5.,22.1731087802709,9.18440237676217));
#34901=CARTESIAN_POINT('',(5.,7.48707131916463,0.440185258433775));
#34902=CARTESIAN_POINT('Ctrl Pts',(5.,7.48707131916463,0.440185258433775));
#34903=CARTESIAN_POINT('Ctrl Pts',(4.68873581543082,7.48707131916463,0.440185258433775));
#34904=CARTESIAN_POINT('Ctrl Pts',(4.35845534789624,7.48402338137256,0.506766716239049));
#34905=CARTESIAN_POINT('Ctrl Pts',(3.75350716939841,7.46156020953612,0.769764179262972));
#34906=CARTESIAN_POINT('Ctrl Pts',(3.47861587184941,7.44093225812105,0.965560498093768));
#34907=CARTESIAN_POINT('Ctrl Pts',(3.04463387982388,7.3703917706363,1.40608039471696));
#34908=CARTESIAN_POINT('Ctrl Pts',(2.85577540978026,7.31555987078622,1.68094905379426));
#34909=CARTESIAN_POINT('Ctrl Pts',(2.60414734335626,7.15493061203946,2.26935538845465));
#34910=CARTESIAN_POINT('Ctrl Pts',(2.54150000000001,7.04816066352038,2.5826794094902));
#34911=CARTESIAN_POINT('Ctrl Pts',(2.54150000000001,6.81003232414892,3.15757207598616));
#34912=CARTESIAN_POINT('Ctrl Pts',(2.60414734335626,6.66397653879082,3.45462337059381));
#34913=CARTESIAN_POINT('Ctrl Pts',(2.85577540978025,6.36149246757615,3.9842715180421));
#34914=CARTESIAN_POINT('Ctrl Pts',(3.04463387982388,6.20590298301627,4.21740501902064));
#34915=CARTESIAN_POINT('Ctrl Pts',(3.47861587184941,5.94428803391508,4.57877928221917));
#34916=CARTESIAN_POINT('Ctrl Pts',(3.75350716939841,5.82042529346604,4.73181435132337));
#34917=CARTESIAN_POINT('Ctrl Pts',(4.35845534789624,5.65034186505947,4.93366550199495));
#34918=CARTESIAN_POINT('Ctrl Pts',(4.68873581543082,5.60541688222548,4.98290091979175));
#34919=CARTESIAN_POINT('Ctrl Pts',(5.31126418456918,5.60541688222548,4.98290091979175));
#34920=CARTESIAN_POINT('Ctrl Pts',(5.64154465210376,5.65034186505947,4.93366550199495));
#34921=CARTESIAN_POINT('Ctrl Pts',(6.24649283060159,5.82042529346604,4.73181435132337));
#34922=CARTESIAN_POINT('Ctrl Pts',(6.52138412815059,5.94428803391508,4.57877928221917));
#34923=CARTESIAN_POINT('Ctrl Pts',(6.95536612017612,6.20590298301627,4.21740501902064));
#34924=CARTESIAN_POINT('Ctrl Pts',(7.14422459021974,6.36149246757615,3.9842715180421));
#34925=CARTESIAN_POINT('Ctrl Pts',(7.39585265664374,6.66397653879082,3.45462337059381));
#34926=CARTESIAN_POINT('Ctrl Pts',(7.45849999999999,6.81003232414892,3.15757207598616));
#34927=CARTESIAN_POINT('Ctrl Pts',(7.45849999999999,7.04816066352038,2.5826794094902));
#34928=CARTESIAN_POINT('Ctrl Pts',(7.39585265664374,7.15493061203946,2.26935538845465));
#34929=CARTESIAN_POINT('Ctrl Pts',(7.14422459021974,7.31555987078622,1.68094905379426));
#34930=CARTESIAN_POINT('Ctrl Pts',(6.95536612017612,7.3703917706363,1.40608039471696));
#34931=CARTESIAN_POINT('Ctrl Pts',(6.52138412815059,7.44093225812105,0.965560498093769));
#34932=CARTESIAN_POINT('Ctrl Pts',(6.24649283060159,7.46156020953611,0.769764179262975));
#34933=CARTESIAN_POINT('Ctrl Pts',(5.64154465210376,7.48402338137256,0.506766716239051));
#34934=CARTESIAN_POINT('Ctrl Pts',(5.31126418456918,7.48707131916463,0.440185258433775));
#34935=CARTESIAN_POINT('Ctrl Pts',(5.,7.48707131916463,0.440185258433775));
#34936=CARTESIAN_POINT('',(5.,22.9972930864807,6.86472946987049));
#34937=CARTESIAN_POINT('',(5.,23.1139359987404,6.91304454608318));
#34938=CARTESIAN_POINT('Ctrl Pts',(5.,22.9972930864807,6.86472946987049));
#34939=CARTESIAN_POINT('Ctrl Pts',(5.30892798186098,22.9972930864807,6.86472946987049));
#34940=CARTESIAN_POINT('Ctrl Pts',(5.63829853703008,22.9797603253307,6.92434139206246));
#34941=CARTESIAN_POINT('Ctrl Pts',(6.24395747678749,22.9057609106853,7.16533358286599));
#34942=CARTESIAN_POINT('Ctrl Pts',(6.52026442354922,22.8489771609384,7.34656970696721));
#34943=CARTESIAN_POINT('Ctrl Pts',(6.95657880152062,22.7112821636813,7.76179785122406));
#34944=CARTESIAN_POINT('Ctrl Pts',(7.1457499860634,22.6211168109853,8.02352301118618));
#34945=CARTESIAN_POINT('Ctrl Pts',(7.39671656426829,22.4112998779956,8.59217580499353));
#34946=CARTESIAN_POINT('Ctrl Pts',(7.45849999999999,22.2913299574281,8.89899120750958));
#34947=CARTESIAN_POINT('Ctrl Pts',(7.45849999999999,22.0548876031137,9.46981354601478));
#34948=CARTESIAN_POINT('Ctrl Pts',(7.39671656426829,21.9227678957938,9.77159634207808));
#34949=CARTESIAN_POINT('Ctrl Pts',(7.1457499860634,21.6690326252767,10.3220575648447));
#34950=CARTESIAN_POINT('Ctrl Pts',(6.95657880152062,21.5477215221798,10.5708817325805));
#34951=CARTESIAN_POINT('Ctrl Pts',(6.52026442354922,21.3514759519323,10.9618574354199));
#34952=CARTESIAN_POINT('Ctrl Pts',(6.24395747678748,21.2634748340916,11.1301629022752));
#34953=CARTESIAN_POINT('Ctrl Pts',(5.63829853703008,21.1453931096609,11.3528956025049));
#34954=CARTESIAN_POINT('Ctrl Pts',(5.30892798186098,21.1156386495415,11.4074451312285));
#34955=CARTESIAN_POINT('Ctrl Pts',(4.69107201813902,21.1156386495415,11.4074451312285));
#34956=CARTESIAN_POINT('Ctrl Pts',(4.36170146296992,21.1453931096609,11.3528956025049));
#34957=CARTESIAN_POINT('Ctrl Pts',(3.75604252321252,21.2634748340916,11.1301629022752));
#34958=CARTESIAN_POINT('Ctrl Pts',(3.47973557645078,21.3514759519323,10.9618574354199));
#34959=CARTESIAN_POINT('Ctrl Pts',(3.04342119847938,21.5477215221798,10.5708817325805));
#34960=CARTESIAN_POINT('Ctrl Pts',(2.8542500139366,21.6690326252767,10.3220575648447));
#34961=CARTESIAN_POINT('Ctrl Pts',(2.60328343573171,21.9227678957938,9.77159634207808));
#34962=CARTESIAN_POINT('Ctrl Pts',(2.54150000000001,22.0548876031137,9.46981354601477));
#34963=CARTESIAN_POINT('Ctrl Pts',(2.54150000000001,22.2913299574281,8.89899120750958));
#34964=CARTESIAN_POINT('Ctrl Pts',(2.60328343573171,22.4112998779956,8.59217580499353));
#34965=CARTESIAN_POINT('Ctrl Pts',(2.85425001393659,22.6211168109853,8.02352301118618));
#34966=CARTESIAN_POINT('Ctrl Pts',(3.04342119847938,22.7112821636813,7.76179785122406));
#34967=CARTESIAN_POINT('Ctrl Pts',(3.47973557645078,22.8489771609384,7.34656970696721));
#34968=CARTESIAN_POINT('Ctrl Pts',(3.75604252321252,22.9057609106853,7.16533358286599));
#34969=CARTESIAN_POINT('Ctrl Pts',(4.36170146296993,22.9797603253307,6.92434139206246));
#34970=CARTESIAN_POINT('Ctrl Pts',(4.69107201813902,22.9972930864807,6.86472946987049));
#34971=CARTESIAN_POINT('Ctrl Pts',(5.,22.9972930864807,6.86472946987049));
#34972=CARTESIAN_POINT('Origin',(10.,13.4350288425444,-13.4350288425444));
#34973=CARTESIAN_POINT('',(0.,13.4350288425444,-10.6850288425444));
#34974=CARTESIAN_POINT('Origin',(0.,13.4350288425444,-13.4350288425444));
#34975=CARTESIAN_POINT('',(10.,13.4350288425444,-10.6850288425444));
#34976=CARTESIAN_POINT('',(10.,13.4350288425444,-10.6850288425444));
#34977=CARTESIAN_POINT('Origin',(10.,13.4350288425444,-13.4350288425444));
#34978=CARTESIAN_POINT('Origin',(10.,19.,0.));
#34979=CARTESIAN_POINT('',(0.,19.,2.74999999999999));
#34980=CARTESIAN_POINT('Origin',(0.,19.,0.));
#34981=CARTESIAN_POINT('',(10.,19.,2.74999999999999));
#34982=CARTESIAN_POINT('',(10.,19.,2.74999999999999));
#34983=CARTESIAN_POINT('Origin',(10.,19.,0.));
#34984=CARTESIAN_POINT('Origin',(10.,13.4350288425444,13.4350288425444));
#34985=CARTESIAN_POINT('',(0.,13.4350288425444,16.1850288425444));
#34986=CARTESIAN_POINT('Origin',(0.,13.4350288425444,13.4350288425444));
#34987=CARTESIAN_POINT('',(10.,13.4350288425444,16.1850288425444));
#34988=CARTESIAN_POINT('',(10.,13.4350288425444,16.1850288425444));
#34989=CARTESIAN_POINT('Origin',(10.,13.4350288425444,13.4350288425444));
#34990=CARTESIAN_POINT('Origin',(10.,-13.4350288425444,13.4350288425444));
#34991=CARTESIAN_POINT('',(0.,-13.4350288425444,16.1850288425444));
#34992=CARTESIAN_POINT('Origin',(0.,-13.4350288425444,13.4350288425444));
#34993=CARTESIAN_POINT('',(10.,-13.4350288425444,16.1850288425444));
#34994=CARTESIAN_POINT('',(10.,-13.4350288425444,16.1850288425444));
#34995=CARTESIAN_POINT('Origin',(10.,-13.4350288425444,13.4350288425444));
#34996=CARTESIAN_POINT('Origin',(10.,-19.,0.));
#34997=CARTESIAN_POINT('',(0.,-19.,2.74999999999999));
#34998=CARTESIAN_POINT('Origin',(0.,-19.,0.));
#34999=CARTESIAN_POINT('',(10.,-19.,2.74999999999999));
#35000=CARTESIAN_POINT('',(10.,-19.,2.74999999999999));
#35001=CARTESIAN_POINT('Origin',(10.,-19.,0.));
#35002=CARTESIAN_POINT('Origin',(10.,-13.4350288425444,-13.4350288425444));
#35003=CARTESIAN_POINT('',(0.,-13.4350288425444,-10.6850288425444));
#35004=CARTESIAN_POINT('Origin',(0.,-13.4350288425444,-13.4350288425444));
#35005=CARTESIAN_POINT('',(10.,-13.4350288425444,-10.6850288425444));
#35006=CARTESIAN_POINT('',(10.,-13.4350288425444,-10.6850288425444));
#35007=CARTESIAN_POINT('Origin',(10.,-13.4350288425444,-13.4350288425444));
#35008=CARTESIAN_POINT('Origin',(-34.1076474136955,0.,0.));
#35009=CARTESIAN_POINT('',(-31.5,-1.71450551880629E-15,-14.));
#35010=CARTESIAN_POINT('Origin',(-31.5,0.,0.));
#35011=CARTESIAN_POINT('',(0.,-1.71450551880629E-15,-14.));
#35012=CARTESIAN_POINT('',(-34.1076474136955,-1.71450551880629E-15,-14.));
#35013=CARTESIAN_POINT('Origin',(0.,0.,0.));
#35014=CARTESIAN_POINT('Origin',(-34.1076474136955,0.,0.));
#35015=CARTESIAN_POINT('',(10.,-1.34711147906209E-15,-11.));
#35016=CARTESIAN_POINT('Origin',(10.,0.,0.));
#35017=CARTESIAN_POINT('',(9.5,-1.34711147906209E-15,-11.));
#35018=CARTESIAN_POINT('',(-34.1076474136955,-1.34711147906209E-15,-11.));
#35019=CARTESIAN_POINT('Origin',(9.5,0.,0.));
#35020=CARTESIAN_POINT('Origin',(-34.1076474136955,0.,0.));
#35021=CARTESIAN_POINT('',(9.50000000000001,-1.31649530908341E-15,-10.75));
#35022=CARTESIAN_POINT('Origin',(9.50000000000001,0.,0.));
#35023=CARTESIAN_POINT('',(10.,-1.31649530908341E-15,-10.75));
#35024=CARTESIAN_POINT('',(-34.1076474136955,-1.31649530908341E-15,-10.75));
#35025=CARTESIAN_POINT('Origin',(10.,0.,0.));
#35026=CARTESIAN_POINT('Origin',(-34.1076474136955,0.,0.));
#35027=CARTESIAN_POINT('',(10.,-9.18485099360515E-16,-7.5));
#35028=CARTESIAN_POINT('Origin',(10.,0.,0.));
#35029=CARTESIAN_POINT('',(-32.,-9.18485099360515E-16,-7.5));
#35030=CARTESIAN_POINT('',(-34.1076474136955,-9.18485099360515E-16,-7.5));
#35031=CARTESIAN_POINT('Origin',(-32.,0.,0.));
#35032=CARTESIAN_POINT('Origin',(-34.1076474136955,0.,0.));
#35033=CARTESIAN_POINT('',(-32.,-1.3164953090834E-15,-10.75));
#35034=CARTESIAN_POINT('Origin',(-32.,0.,0.));
#35035=CARTESIAN_POINT('',(-31.5,-1.3164953090834E-15,-10.75));
#35036=CARTESIAN_POINT('',(-34.1076474136955,-1.3164953090834E-15,-10.75));
#35037=CARTESIAN_POINT('Origin',(-31.5,0.,0.));
#35038=CARTESIAN_POINT('Origin',(-34.1076474136955,0.,0.));
#35039=CARTESIAN_POINT('',(-31.5,-1.34711147906209E-15,-11.));
#35040=CARTESIAN_POINT('Origin',(-31.5,0.,0.));
#35041=CARTESIAN_POINT('',(-32.,-1.34711147906209E-15,-11.));
#35042=CARTESIAN_POINT('',(-34.1076474136955,-1.34711147906209E-15,-11.));
#35043=CARTESIAN_POINT('Origin',(-32.,0.,0.));
#35044=CARTESIAN_POINT('Origin',(-31.5,0.,0.));
#35045=CARTESIAN_POINT('',(-32.,-1.65327317884893E-15,-13.5));
#35046=CARTESIAN_POINT('Origin',(-32.,0.,0.));
#35047=CARTESIAN_POINT('Origin',(-31.5,-1.65327317884893E-15,-13.5));
#35048=CARTESIAN_POINT('Origin',(10.,23.,0.));
#35049=CARTESIAN_POINT('',(10.,11.3578166916005,20.));
#35050=CARTESIAN_POINT('',(10.,-11.3578166915893,20.));
#35051=CARTESIAN_POINT('',(10.,24.,20.));
#35052=CARTESIAN_POINT('',(10.,-11.3578166916005,-20.));
#35053=CARTESIAN_POINT('Origin',(10.,0.,0.));
#35054=CARTESIAN_POINT('',(10.,11.3578166916005,-20.));
#35055=CARTESIAN_POINT('',(10.,24.,-20.));
#35056=CARTESIAN_POINT('Origin',(10.,0.,0.));
#35057=CARTESIAN_POINT('Origin',(9.,0.,0.));
#35058=CARTESIAN_POINT('',(9.,-13.2664991614216,20.));
#35059=CARTESIAN_POINT('Ctrl Pts',(9.,-13.2664991614216,20.));
#35060=CARTESIAN_POINT('Ctrl Pts',(9.09995111742602,-13.2664991614216,20.));
#35061=CARTESIAN_POINT('Ctrl Pts',(9.21480544093045,-13.231938929479,20.));
#35062=CARTESIAN_POINT('Ctrl Pts',(9.42146594446646,-13.1132046912743,20.));
#35063=CARTESIAN_POINT('Ctrl Pts',(9.53638021469469,-12.9933163967994,20.));
#35064=CARTESIAN_POINT('Ctrl Pts',(9.7313641110186,-12.7122458236771,20.));
#35065=CARTESIAN_POINT('Ctrl Pts',(9.82490699559395,-12.4864240538002,20.));
#35066=CARTESIAN_POINT('Ctrl Pts',(9.96053133753905,-12.0059148948793,20.));
#35067=CARTESIAN_POINT('Ctrl Pts',(10.,-11.6534080045929,20.));
#35068=CARTESIAN_POINT('Ctrl Pts',(10.,-11.3578166916006,20.));
#35069=CARTESIAN_POINT('',(9.,-13.2664991614216,-20.));
#35070=CARTESIAN_POINT('Origin',(9.,0.,0.));
#35071=CARTESIAN_POINT('Ctrl Pts',(10.,-11.3578166916006,-20.));
#35072=CARTESIAN_POINT('Ctrl Pts',(10.,-11.6534080045929,-20.));
#35073=CARTESIAN_POINT('Ctrl Pts',(9.96053133753905,-12.0059148948793,-20.));
#35074=CARTESIAN_POINT('Ctrl Pts',(9.82490699559395,-12.4864240538002,-20.));
#35075=CARTESIAN_POINT('Ctrl Pts',(9.7313641110186,-12.7122458236771,-20.));
#35076=CARTESIAN_POINT('Ctrl Pts',(9.53638021469469,-12.9933163967994,-20.));
#35077=CARTESIAN_POINT('Ctrl Pts',(9.42146594446646,-13.1132046912743,-20.));
#35078=CARTESIAN_POINT('Ctrl Pts',(9.21480544093045,-13.231938929479,-20.));
#35079=CARTESIAN_POINT('Ctrl Pts',(9.09995111742602,-13.2664991614216,-20.));
#35080=CARTESIAN_POINT('Ctrl Pts',(9.,-13.2664991614216,-20.));
#35081=CARTESIAN_POINT('Origin',(9.,0.,0.));
#35082=CARTESIAN_POINT('',(9.,13.2664991614216,20.));
#35083=CARTESIAN_POINT('Ctrl Pts',(10.,11.3578166916006,20.));
#35084=CARTESIAN_POINT('Ctrl Pts',(10.,11.6534080045929,20.));
#35085=CARTESIAN_POINT('Ctrl Pts',(9.96053133753905,12.0059148948794,20.));
#35086=CARTESIAN_POINT('Ctrl Pts',(9.82490699559395,12.4864240538002,20.));
#35087=CARTESIAN_POINT('Ctrl Pts',(9.7313641110186,12.7122458236771,20.));
#35088=CARTESIAN_POINT('Ctrl Pts',(9.53638021469469,12.9933163967994,20.));
#35089=CARTESIAN_POINT('Ctrl Pts',(9.42146594446646,13.1132046912743,20.));
#35090=CARTESIAN_POINT('Ctrl Pts',(9.21480544093045,13.231938929479,20.));
#35091=CARTESIAN_POINT('Ctrl Pts',(9.09995111742602,13.2664991614216,20.));
#35092=CARTESIAN_POINT('Ctrl Pts',(9.,13.2664991614216,20.));
#35093=CARTESIAN_POINT('',(9.,13.2664991614216,-20.));
#35094=CARTESIAN_POINT('Ctrl Pts',(9.,13.2664991614216,-20.));
#35095=CARTESIAN_POINT('Ctrl Pts',(9.09995111742602,13.2664991614216,-20.));
#35096=CARTESIAN_POINT('Ctrl Pts',(9.21480544093045,13.231938929479,-20.));
#35097=CARTESIAN_POINT('Ctrl Pts',(9.42146594446646,13.1132046912743,-20.));
#35098=CARTESIAN_POINT('Ctrl Pts',(9.53638021469469,12.9933163967994,-20.));
#35099=CARTESIAN_POINT('Ctrl Pts',(9.7313641110186,12.7122458236771,-20.));
#35100=CARTESIAN_POINT('Ctrl Pts',(9.82490699559395,12.4864240538002,-20.));
#35101=CARTESIAN_POINT('Ctrl Pts',(9.96053133753905,12.0059148948794,-20.));
#35102=CARTESIAN_POINT('Ctrl Pts',(10.,11.6534080045929,-20.));
#35103=CARTESIAN_POINT('Ctrl Pts',(10.,11.3578166916006,-20.));
#35104=CARTESIAN_POINT('Origin',(9.,0.,0.));
#35105=CARTESIAN_POINT('Origin',(-34.1076474136955,0.,0.));
#35106=CARTESIAN_POINT('',(0.999999999999992,13.2664991614216,-20.));
#35107=CARTESIAN_POINT('',(-34.1076474136955,13.2664991614216,-20.));
#35108=CARTESIAN_POINT('',(0.999999999999971,13.2664991614216,20.));
#35109=CARTESIAN_POINT('Origin',(1.,0.,0.));
#35110=CARTESIAN_POINT('',(-34.1076474136955,13.2664991614216,20.));
#35111=CARTESIAN_POINT('Origin',(-34.1076474136955,0.,0.));
#35112=CARTESIAN_POINT('',(1.,-13.2664991614216,-20.));
#35113=CARTESIAN_POINT('',(-34.1076474136955,-13.2664991614216,-20.));
#35114=CARTESIAN_POINT('',(1.,-13.2664991614216,20.));
#35115=CARTESIAN_POINT('',(-34.1076474136955,-13.2664991614216,20.));
#35116=CARTESIAN_POINT('Origin',(1.,0.,0.));
#35117=CARTESIAN_POINT('Origin',(1.,0.,0.));
#35118=CARTESIAN_POINT('',(1.73472347597681E-15,-11.3578166916005,20.));
#35119=CARTESIAN_POINT('Ctrl Pts',(-4.16333634234434E-16,-11.3578166916005,
20.));
#35120=CARTESIAN_POINT('Ctrl Pts',(-8.757748284231E-16,-11.6534080045929,
20.));
#35121=CARTESIAN_POINT('Ctrl Pts',(0.039468662460955,-12.0059148948793,
20.));
#35122=CARTESIAN_POINT('Ctrl Pts',(0.175093004406055,-12.4864240538002,
20.));
#35123=CARTESIAN_POINT('Ctrl Pts',(0.268635888981406,-12.7122458236771,
20.));
#35124=CARTESIAN_POINT('Ctrl Pts',(0.463619785305314,-12.9933163967994,
20.));
#35125=CARTESIAN_POINT('Ctrl Pts',(0.578534055533546,-13.1132046912743,
20.));
#35126=CARTESIAN_POINT('Ctrl Pts',(0.785194559069557,-13.231938929479,20.));
#35127=CARTESIAN_POINT('Ctrl Pts',(0.900048882573979,-13.2664991614216,
20.));
#35128=CARTESIAN_POINT('Ctrl Pts',(1.,-13.2664991614216,20.));
#35129=CARTESIAN_POINT('',(0.,-11.3578166916005,-20.));
#35130=CARTESIAN_POINT('Origin',(0.,0.,0.));
#35131=CARTESIAN_POINT('Ctrl Pts',(1.,-13.2664991614216,-20.));
#35132=CARTESIAN_POINT('Ctrl Pts',(0.900048882573979,-13.2664991614216,
-20.));
#35133=CARTESIAN_POINT('Ctrl Pts',(0.785194559069558,-13.231938929479,-20.));
#35134=CARTESIAN_POINT('Ctrl Pts',(0.578534055533547,-13.1132046912743,
-20.));
#35135=CARTESIAN_POINT('Ctrl Pts',(0.463619785305315,-12.9933163967994,
-20.));
#35136=CARTESIAN_POINT('Ctrl Pts',(0.268635888981407,-12.7122458236771,
-20.));
#35137=CARTESIAN_POINT('Ctrl Pts',(0.175093004406055,-12.4864240538002,
-20.));
#35138=CARTESIAN_POINT('Ctrl Pts',(0.0394686624609555,-12.0059148948793,
-20.));
#35139=CARTESIAN_POINT('Ctrl Pts',(-1.0726781973611E-15,-11.6534080045929,
-20.));
#35140=CARTESIAN_POINT('Ctrl Pts',(-4.16333634234433E-16,-11.3578166916006,
-20.));
#35141=CARTESIAN_POINT('Origin',(1.,0.,0.));
#35142=CARTESIAN_POINT('',(0.,11.3578166916005,20.));
#35143=CARTESIAN_POINT('Ctrl Pts',(0.999999999999971,13.2664991614216,20.));
#35144=CARTESIAN_POINT('Ctrl Pts',(0.90004888257395,13.2664991614216,20.));
#35145=CARTESIAN_POINT('Ctrl Pts',(0.785194559069557,13.231938929479,20.));
#35146=CARTESIAN_POINT('Ctrl Pts',(0.578534055533546,13.1132046912743,20.));
#35147=CARTESIAN_POINT('Ctrl Pts',(0.463619785305314,12.9933163967994,20.));
#35148=CARTESIAN_POINT('Ctrl Pts',(0.268635888981406,12.7122458236771,20.));
#35149=CARTESIAN_POINT('Ctrl Pts',(0.175093004406055,12.4864240538002,20.));
#35150=CARTESIAN_POINT('Ctrl Pts',(0.039468662460955,12.0059148948794,20.));
#35151=CARTESIAN_POINT('Ctrl Pts',(-4.16333634234434E-16,11.6534080045929,
20.));
#35152=CARTESIAN_POINT('Ctrl Pts',(-4.16333634234434E-16,11.3578166916006,
20.));
#35153=CARTESIAN_POINT('',(1.73472347597681E-15,11.3578166916005,-20.));
#35154=CARTESIAN_POINT('Ctrl Pts',(-4.16333634234434E-16,11.3578166916006,
-20.));
#35155=CARTESIAN_POINT('Ctrl Pts',(-1.05562532344124E-15,11.6534080045929,
-20.));
#35156=CARTESIAN_POINT('Ctrl Pts',(0.0394686624609556,12.0059148948794,
-20.));
#35157=CARTESIAN_POINT('Ctrl Pts',(0.175093004406055,12.4864240538002,-20.));
#35158=CARTESIAN_POINT('Ctrl Pts',(0.268635888981407,12.7122458236771,-20.));
#35159=CARTESIAN_POINT('Ctrl Pts',(0.463619785305315,12.9933163967994,-20.));
#35160=CARTESIAN_POINT('Ctrl Pts',(0.578534055533547,13.1132046912743,-20.));
#35161=CARTESIAN_POINT('Ctrl Pts',(0.785194559069558,13.231938929479,-20.));
#35162=CARTESIAN_POINT('Ctrl Pts',(0.900048882573979,13.2664991614216,-20.));
#35163=CARTESIAN_POINT('Ctrl Pts',(1.,13.2664991614216,-20.));
#35164=CARTESIAN_POINT('Origin',(0.,0.,0.));
#35165=CARTESIAN_POINT('Origin',(0.,14.,0.));
#35166=CARTESIAN_POINT('',(0.,14.,20.));
#35167=CARTESIAN_POINT('',(0.,14.,-20.));
#35168=CARTESIAN_POINT('Origin',(-32.,11.,0.));
#35169=CARTESIAN_POINT('Origin',(-31.5,11.,0.));
#35170=CARTESIAN_POINT('Origin',(-32.,10.75,0.));
#35171=CARTESIAN_POINT('Origin',(10.,10.75,0.));
#35172=CARTESIAN_POINT('Origin',(9.5,10.75,0.));
#35173=CARTESIAN_POINT('Origin',(1.73472347597681E-15,24.,-20.));
#35174=CARTESIAN_POINT('Origin',(1.73472347597681E-15,24.,20.));
#57007=UNCERTAINTY_MEASURE_WITH_UNIT(LENGTH_MEASURE(0.01),#57080,
'DISTANCE_ACCURACY_VALUE',
'Maximum model space distance between geometric entities at asserted c
onnectivities');
#57040=UNCERTAINTY_MEASURE_WITH_UNIT(LENGTH_MEASURE(0.01),#57080,
'DISTANCE_ACCURACY_VALUE',
'Maximum model space distance between geometric entities at asserted c
onnectivities');
#57046=(
GEOMETRIC_REPRESENTATION_CONTEXT(3)
GLOBAL_UNCERTAINTY_ASSIGNED_CONTEXT((#57007))
GLOBAL_UNIT_ASSIGNED_CONTEXT((#57080,#57082,#57083))
REPRESENTATION_CONTEXT('','3D')
);
#57079=(
GEOMETRIC_REPRESENTATION_CONTEXT(3)
GLOBAL_UNCERTAINTY_ASSIGNED_CONTEXT((#57040))
GLOBAL_UNIT_ASSIGNED_CONTEXT((#57080,#57082,#57083))
REPRESENTATION_CONTEXT('','3D')
);
#57080=(
LENGTH_UNIT()
NAMED_UNIT(*)
SI_UNIT(.MILLI.,.METRE.)
);
#57082=(
NAMED_UNIT(*)
PLANE_ANGLE_UNIT()
SI_UNIT($,.RADIAN.)
);
#57083=(
NAMED_UNIT(*)
SI_UNIT($,.STERADIAN.)
SOLID_ANGLE_UNIT()
);
#57089=SHAPE_DEFINITION_REPRESENTATION(#57127,#57254);
#57127=PRODUCT_DEFINITION_SHAPE('',$,#57293);
#57254=SHAPE_REPRESENTATION('',(#24990),#57046);
#57287=PRODUCT_DEFINITION_CONTEXT('part definition',#57403,'design');
#57293=PRODUCT_DEFINITION('Ball Screw Nut','Ball Screw Nut',#57331,#57287);
#57331=PRODUCT_DEFINITION_FORMATION('',$,#57410);
#57403=APPLICATION_CONTEXT(
'Core Data for Automotive Mechanical Design Process');
#57404=PRODUCT_CONTEXT('part definition',#57403,'mechanical');
#57410=PRODUCT('Ball Screw Nut','Ball Screw Nut',$,(#57404));
#57444=PRESENTATION_STYLE_ASSIGNMENT((#57446));
#57446=SURFACE_STYLE_USAGE(.BOTH.,#57448);
#57448=SURFACE_SIDE_STYLE('',(#57450));
#57450=SURFACE_STYLE_FILL_AREA(#57452);
#57452=FILL_AREA_STYLE('Opaque(202,209,238)',(#57454));
#57454=FILL_AREA_STYLE_COLOUR('Opaque(202,209,238)',#57456);
#57456=COLOUR_RGB('Opaque(202,209,238)',0.792156862745098,0.819607843137255,
0.933333333333333);
ENDSEC;
END-ISO-10303-21;
